ISO-10303-21;
HEADER;
/* Generated by software containing ST-Developer
 * from STEP Tools, Inc. (www.steptools.com) 
 */

FILE_DESCRIPTION(
/* description */ (''),
/* implementation_level */ '2;1');

FILE_NAME(
/* name */ 'Nut_02.step',
/* time_stamp */ '2026-10-05T16:20:14-07:00',
/* author */ (''),
/* organization */ (''),
/* preprocessor_version */ 'ST-DEVELOPER v20.2',
/* originating_system */ 'Autodesk Translation Framework v15.15.0.0',
/* authorisation */ '');

FILE_SCHEMA (('AUTOMOTIVE_DESIGN { 1 0 10303 214 3 1 1 }'));
ENDSEC;

DATA;
#10=MECHANICAL_DESIGN_GEOMETRIC_PRESENTATION_REPRESENTATION('',(#252),#23577);
#234=SHAPE_REPRESENTATION_RELATIONSHIP('SRR','None',#23617,#243);
#243=ADVANCED_BREP_SHAPE_REPRESENTATION('',(#261),#23573);
#252=STYLED_ITEM('',(#23666),#261);
#261=MANIFOLD_SOLID_BREP('Body1',#4162);
#284=FACE_BOUND('',#767,.T.);
#285=FACE_BOUND('',#769,.T.);
#353=PLANE('',#4477);
#354=PLANE('',#4478);
#355=PLANE('',#4479);
#356=PLANE('',#4480);
#357=PLANE('',#4481);
#358=PLANE('',#4482);
#359=PLANE('',#4483);
#360=PLANE('',#4484);
#514=FACE_OUTER_BOUND('',#759,.T.);
#515=FACE_OUTER_BOUND('',#760,.T.);
#516=FACE_OUTER_BOUND('',#761,.T.);
#517=FACE_OUTER_BOUND('',#762,.T.);
#518=FACE_OUTER_BOUND('',#763,.T.);
#519=FACE_OUTER_BOUND('',#764,.T.);
#520=FACE_OUTER_BOUND('',#765,.T.);
#521=FACE_OUTER_BOUND('',#766,.T.);
#522=FACE_OUTER_BOUND('',#768,.T.);
#759=EDGE_LOOP('',(#3345,#3346,#3347,#3348));
#760=EDGE_LOOP('',(#3349,#3350,#3351,#3352));
#761=EDGE_LOOP('',(#3353,#3354,#3355,#3356));
#762=EDGE_LOOP('',(#3357,#3358,#3359,#3360));
#763=EDGE_LOOP('',(#3361,#3362,#3363,#3364));
#764=EDGE_LOOP('',(#3365,#3366,#3367,#3368));
#765=EDGE_LOOP('',(#3369,#3370,#3371,#3372));
#766=EDGE_LOOP('',(#3373,#3374,#3375,#3376,#3377,#3378));
#767=EDGE_LOOP('',(#3379));
#768=EDGE_LOOP('',(#3380,#3381,#3382,#3383,#3384,#3385));
#769=EDGE_LOOP('',(#3386));
#1050=LINE('',#21509,#1335);
#1051=LINE('',#21514,#1336);
#1052=LINE('',#21516,#1337);
#1053=LINE('',#21518,#1338);
#1054=LINE('',#21519,#1339);
#1055=LINE('',#21522,#1340);
#1056=LINE('',#21524,#1341);
#1057=LINE('',#21525,#1342);
#1058=LINE('',#21528,#1343);
#1059=LINE('',#21530,#1344);
#1060=LINE('',#21531,#1345);
#1061=LINE('',#21534,#1346);
#1062=LINE('',#21536,#1347);
#1063=LINE('',#21537,#1348);
#1064=LINE('',#21540,#1349);
#1065=LINE('',#21542,#1350);
#1066=LINE('',#21543,#1351);
#1067=LINE('',#21545,#1352);
#1068=LINE('',#21546,#1353);
#1335=VECTOR('',#5261,2.5);
#1336=VECTOR('',#5266,9.99999999999999);
#1337=VECTOR('',#5267,10.);
#1338=VECTOR('',#5268,9.99999999999999);
#1339=VECTOR('',#5269,10.);
#1340=VECTOR('',#5272,10.);
#1341=VECTOR('',#5273,10.);
#1342=VECTOR('',#5274,10.);
#1343=VECTOR('',#5277,10.);
#1344=VECTOR('',#5278,10.);
#1345=VECTOR('',#5279,10.);
#1346=VECTOR('',#5282,10.);
#1347=VECTOR('',#5283,10.);
#1348=VECTOR('',#5284,10.);
#1349=VECTOR('',#5287,10.);
#1350=VECTOR('',#5288,10.);
#1351=VECTOR('',#5289,10.);
#1352=VECTOR('',#5292,10.);
#1353=VECTOR('',#5293,10.);
#1534=CIRCLE('',#4475,2.5);
#1535=CIRCLE('',#4476,2.5);
#1879=VERTEX_POINT('',#21506);
#1880=VERTEX_POINT('',#21508);
#1881=VERTEX_POINT('',#21512);
#1882=VERTEX_POINT('',#21513);
#1883=VERTEX_POINT('',#21515);
#1884=VERTEX_POINT('',#21517);
#1885=VERTEX_POINT('',#21521);
#1886=VERTEX_POINT('',#21523);
#1887=VERTEX_POINT('',#21527);
#1888=VERTEX_POINT('',#21529);
#1889=VERTEX_POINT('',#21533);
#1890=VERTEX_POINT('',#21535);
#1891=VERTEX_POINT('',#21539);
#1892=VERTEX_POINT('',#21541);
#2389=EDGE_CURVE('',#1879,#1879,#1534,.T.);
#2390=EDGE_CURVE('',#1879,#1880,#1050,.T.);
#2391=EDGE_CURVE('',#1880,#1880,#1535,.T.);
#2392=EDGE_CURVE('',#1881,#1882,#1051,.T.);
#2393=EDGE_CURVE('',#1881,#1883,#1052,.T.);
#2394=EDGE_CURVE('',#1884,#1883,#1053,.T.);
#2395=EDGE_CURVE('',#1882,#1884,#1054,.T.);
#2396=EDGE_CURVE('',#1882,#1885,#1055,.T.);
#2397=EDGE_CURVE('',#1886,#1884,#1056,.T.);
#2398=EDGE_CURVE('',#1885,#1886,#1057,.T.);
#2399=EDGE_CURVE('',#1885,#1887,#1058,.T.);
#2400=EDGE_CURVE('',#1888,#1886,#1059,.T.);
#2401=EDGE_CURVE('',#1887,#1888,#1060,.T.);
#2402=EDGE_CURVE('',#1887,#1889,#1061,.T.);
#2403=EDGE_CURVE('',#1890,#1888,#1062,.T.);
#2404=EDGE_CURVE('',#1889,#1890,#1063,.T.);
#2405=EDGE_CURVE('',#1889,#1891,#1064,.T.);
#2406=EDGE_CURVE('',#1892,#1890,#1065,.T.);
#2407=EDGE_CURVE('',#1891,#1892,#1066,.T.);
#2408=EDGE_CURVE('',#1891,#1881,#1067,.T.);
#2409=EDGE_CURVE('',#1883,#1892,#1068,.T.);
#3345=ORIENTED_EDGE('',*,*,#2389,.F.);
#3346=ORIENTED_EDGE('',*,*,#2390,.T.);
#3347=ORIENTED_EDGE('',*,*,#2391,.F.);
#3348=ORIENTED_EDGE('',*,*,#2390,.F.);
#3349=ORIENTED_EDGE('',*,*,#2392,.F.);
#3350=ORIENTED_EDGE('',*,*,#2393,.T.);
#3351=ORIENTED_EDGE('',*,*,#2394,.F.);
#3352=ORIENTED_EDGE('',*,*,#2395,.F.);
#3353=ORIENTED_EDGE('',*,*,#2396,.F.);
#3354=ORIENTED_EDGE('',*,*,#2395,.T.);
#3355=ORIENTED_EDGE('',*,*,#2397,.F.);
#3356=ORIENTED_EDGE('',*,*,#2398,.F.);
#3357=ORIENTED_EDGE('',*,*,#2399,.F.);
#3358=ORIENTED_EDGE('',*,*,#2398,.T.);
#3359=ORIENTED_EDGE('',*,*,#2400,.F.);
#3360=ORIENTED_EDGE('',*,*,#2401,.F.);
#3361=ORIENTED_EDGE('',*,*,#2402,.F.);
#3362=ORIENTED_EDGE('',*,*,#2401,.T.);
#3363=ORIENTED_EDGE('',*,*,#2403,.F.);
#3364=ORIENTED_EDGE('',*,*,#2404,.F.);
#3365=ORIENTED_EDGE('',*,*,#2405,.F.);
#3366=ORIENTED_EDGE('',*,*,#2404,.T.);
#3367=ORIENTED_EDGE('',*,*,#2406,.F.);
#3368=ORIENTED_EDGE('',*,*,#2407,.F.);
#3369=ORIENTED_EDGE('',*,*,#2408,.F.);
#3370=ORIENTED_EDGE('',*,*,#2407,.T.);
#3371=ORIENTED_EDGE('',*,*,#2409,.F.);
#3372=ORIENTED_EDGE('',*,*,#2393,.F.);
#3373=ORIENTED_EDGE('',*,*,#2408,.T.);
#3374=ORIENTED_EDGE('',*,*,#2392,.T.);
#3375=ORIENTED_EDGE('',*,*,#2396,.T.);
#3376=ORIENTED_EDGE('',*,*,#2399,.T.);
#3377=ORIENTED_EDGE('',*,*,#2402,.T.);
#3378=ORIENTED_EDGE('',*,*,#2405,.T.);
#3379=ORIENTED_EDGE('',*,*,#2389,.T.);
#3380=ORIENTED_EDGE('',*,*,#2409,.T.);
#3381=ORIENTED_EDGE('',*,*,#2406,.T.);
#3382=ORIENTED_EDGE('',*,*,#2403,.T.);
#3383=ORIENTED_EDGE('',*,*,#2400,.T.);
#3384=ORIENTED_EDGE('',*,*,#2397,.T.);
#3385=ORIENTED_EDGE('',*,*,#2394,.T.);
#3386=ORIENTED_EDGE('',*,*,#2391,.T.);
#3898=CYLINDRICAL_SURFACE('',#4474,2.5);
#4049=ADVANCED_FACE('',(#514),#3898,.F.);
#4050=ADVANCED_FACE('',(#515),#353,.T.);
#4051=ADVANCED_FACE('',(#516),#354,.T.);
#4052=ADVANCED_FACE('',(#517),#355,.T.);
#4053=ADVANCED_FACE('',(#518),#356,.T.);
#4054=ADVANCED_FACE('',(#519),#357,.T.);
#4055=ADVANCED_FACE('',(#520),#358,.T.);
#4056=ADVANCED_FACE('',(#521,#284),#359,.T.);
#4057=ADVANCED_FACE('',(#522,#285),#360,.F.);
#4162=CLOSED_SHELL('',(#4049,#4050,#4051,#4052,#4053,#4054,#4055,#4056,
#4057));
#4473=AXIS2_PLACEMENT_3D('',#21504,#5255,#5256);
#4474=AXIS2_PLACEMENT_3D('',#21505,#5257,#5258);
#4475=AXIS2_PLACEMENT_3D('',#21507,#5259,#5260);
#4476=AXIS2_PLACEMENT_3D('',#21510,#5262,#5263);
#4477=AXIS2_PLACEMENT_3D('',#21511,#5264,#5265);
#4478=AXIS2_PLACEMENT_3D('',#21520,#5270,#5271);
#4479=AXIS2_PLACEMENT_3D('',#21526,#5275,#5276);
#4480=AXIS2_PLACEMENT_3D('',#21532,#5280,#5281);
#4481=AXIS2_PLACEMENT_3D('',#21538,#5285,#5286);
#4482=AXIS2_PLACEMENT_3D('',#21544,#5290,#5291);
#4483=AXIS2_PLACEMENT_3D('',#21547,#5294,#5295);
#4484=AXIS2_PLACEMENT_3D('',#21548,#5296,#5297);
#5255=DIRECTION('axis',(0.,0.,1.));
#5256=DIRECTION('refdir',(1.,0.,0.));
#5257=DIRECTION('center_axis',(0.,0.,-1.));
#5258=DIRECTION('ref_axis',(-1.,0.,0.));
#5259=DIRECTION('center_axis',(0.,0.,-1.));
#5260=DIRECTION('ref_axis',(-1.,0.,0.));
#5261=DIRECTION('',(0.,0.,-1.));
#5262=DIRECTION('center_axis',(0.,0.,1.));
#5263=DIRECTION('ref_axis',(-1.,0.,0.));
#5264=DIRECTION('center_axis',(0.866025403784439,-0.5,0.));
#5265=DIRECTION('ref_axis',(-0.5,-0.866025403784439,0.));
#5266=DIRECTION('',(0.5,0.866025403784439,0.));
#5267=DIRECTION('',(0.,0.,-1.));
#5268=DIRECTION('',(-0.5,-0.866025403784439,0.));
#5269=DIRECTION('',(0.,0.,-1.));
#5270=DIRECTION('center_axis',(0.866025403784439,0.5,0.));
#5271=DIRECTION('ref_axis',(0.5,-0.866025403784439,0.));
#5272=DIRECTION('',(-0.5,0.866025403784439,0.));
#5273=DIRECTION('',(0.5,-0.866025403784439,0.));
#5274=DIRECTION('',(0.,0.,-1.));
#5275=DIRECTION('center_axis',(4.80740671595891E-16,1.,0.));
#5276=DIRECTION('ref_axis',(1.,-4.80740671595891E-16,0.));
#5277=DIRECTION('',(-1.,4.80740671595891E-16,0.));
#5278=DIRECTION('',(1.,-4.80740671595891E-16,0.));
#5279=DIRECTION('',(0.,0.,-1.));
#5280=DIRECTION('center_axis',(-0.866025403784438,0.500000000000001,0.));
#5281=DIRECTION('ref_axis',(0.500000000000001,0.866025403784438,0.));
#5282=DIRECTION('',(-0.500000000000001,-0.866025403784438,0.));
#5283=DIRECTION('',(0.500000000000001,0.866025403784438,0.));
#5284=DIRECTION('',(0.,0.,-1.));
#5285=DIRECTION('center_axis',(-0.866025403784439,-0.499999999999999,0.));
#5286=DIRECTION('ref_axis',(-0.499999999999999,0.866025403784439,0.));
#5287=DIRECTION('',(0.499999999999999,-0.866025403784439,0.));
#5288=DIRECTION('',(-0.499999999999999,0.866025403784439,0.));
#5289=DIRECTION('',(0.,0.,-1.));
#5290=DIRECTION('center_axis',(-1.20185167898973E-16,-1.,0.));
#5291=DIRECTION('ref_axis',(-1.,1.20185167898973E-16,0.));
#5292=DIRECTION('',(1.,-1.20185167898973E-16,0.));
#5293=DIRECTION('',(-1.,1.20185167898973E-16,0.));
#5294=DIRECTION('center_axis',(0.,0.,1.));
#5295=DIRECTION('ref_axis',(-1.,0.,0.));
#5296=DIRECTION('center_axis',(0.,0.,1.));
#5297=DIRECTION('ref_axis',(-1.,0.,0.));
#21504=CARTESIAN_POINT('',(0.,0.,0.));
#21505=CARTESIAN_POINT('Origin',(5.09382715545311,0.,-0.793637468833951));
#21506=CARTESIAN_POINT('',(7.59382715545311,3.06161699786838E-16,-0.793637468833951));
#21507=CARTESIAN_POINT('Origin',(5.09382715545311,0.,-0.793637468833951));
#21508=CARTESIAN_POINT('',(7.59382715545311,3.06161699786838E-16,-3.79363746883395));
#21509=CARTESIAN_POINT('',(7.59382715545311,-3.06161699786838E-16,-0.793637468833951));
#21510=CARTESIAN_POINT('Origin',(5.09382715545311,0.,-3.79363746883395));
#21511=CARTESIAN_POINT('Origin',(9.71262930897012,-1.11022302462516E-15,
-0.793637468833951));
#21512=CARTESIAN_POINT('',(7.40322823221161,-4.,-0.793637468833951));
#21513=CARTESIAN_POINT('',(9.71262930897012,-1.11022302462516E-15,-0.793637468833951));
#21514=CARTESIAN_POINT('',(7.40322823221161,-4.,-0.793637468833951));
#21515=CARTESIAN_POINT('',(7.40322823221161,-4.,-3.79363746883395));
#21516=CARTESIAN_POINT('',(7.40322823221161,-4.,-0.793637468833951));
#21517=CARTESIAN_POINT('',(9.71262930897012,-1.11022302462516E-15,-3.79363746883395));
#21518=CARTESIAN_POINT('',(7.40322823221161,-4.,-3.79363746883395));
#21519=CARTESIAN_POINT('',(9.71262930897012,-1.11022302462516E-15,-0.793637468833951));
#21520=CARTESIAN_POINT('Origin',(7.40322823221161,4.,-0.793637468833951));
#21521=CARTESIAN_POINT('',(7.40322823221161,4.,-0.793637468833951));
#21522=CARTESIAN_POINT('',(9.71262930897012,-1.11022302462516E-15,-0.793637468833951));
#21523=CARTESIAN_POINT('',(7.40322823221161,4.,-3.79363746883395));
#21524=CARTESIAN_POINT('',(9.71262930897012,-1.11022302462516E-15,-3.79363746883395));
#21525=CARTESIAN_POINT('',(7.40322823221161,4.,-0.793637468833951));
#21526=CARTESIAN_POINT('Origin',(2.78442607869461,4.,-0.793637468833951));
#21527=CARTESIAN_POINT('',(2.78442607869461,4.,-0.793637468833951));
#21528=CARTESIAN_POINT('',(7.40322823221161,4.,-0.793637468833951));
#21529=CARTESIAN_POINT('',(2.78442607869461,4.,-3.79363746883395));
#21530=CARTESIAN_POINT('',(7.40322823221161,4.,-3.79363746883395));
#21531=CARTESIAN_POINT('',(2.78442607869461,4.,-0.793637468833951));
#21532=CARTESIAN_POINT('Origin',(0.4750250019361,2.77555756156289E-15,-0.793637468833951));
#21533=CARTESIAN_POINT('',(0.4750250019361,2.77555756156289E-15,-0.793637468833951));
#21534=CARTESIAN_POINT('',(2.78442607869461,4.,-0.793637468833951));
#21535=CARTESIAN_POINT('',(0.4750250019361,2.77555756156289E-15,-3.79363746883395));
#21536=CARTESIAN_POINT('',(2.78442607869461,4.,-3.79363746883395));
#21537=CARTESIAN_POINT('',(0.4750250019361,2.77555756156289E-15,-0.793637468833951));
#21538=CARTESIAN_POINT('Origin',(2.7844260786946,-4.,-0.793637468833951));
#21539=CARTESIAN_POINT('',(2.7844260786946,-4.,-0.793637468833951));
#21540=CARTESIAN_POINT('',(0.4750250019361,2.77555756156289E-15,-0.793637468833951));
#21541=CARTESIAN_POINT('',(2.7844260786946,-4.,-3.79363746883395));
#21542=CARTESIAN_POINT('',(0.4750250019361,2.77555756156289E-15,-3.79363746883395));
#21543=CARTESIAN_POINT('',(2.7844260786946,-4.,-0.793637468833951));
#21544=CARTESIAN_POINT('Origin',(7.40322823221161,-4.,-0.793637468833951));
#21545=CARTESIAN_POINT('',(2.7844260786946,-4.,-0.793637468833951));
#21546=CARTESIAN_POINT('',(2.7844260786946,-4.,-3.79363746883395));
#21547=CARTESIAN_POINT('Origin',(5.09382715545311,5.55111512312578E-16,
-0.793637468833951));
#21548=CARTESIAN_POINT('Origin',(5.09382715545311,5.55111512312578E-16,
-3.79363746883395));
#23562=UNCERTAINTY_MEASURE_WITH_UNIT(LENGTH_MEASURE(0.01),#23578,
'DISTANCE_ACCURACY_VALUE',
'Maximum model space distance between geometric entities at asserted c
onnectivities');
#23566=UNCERTAINTY_MEASURE_WITH_UNIT(LENGTH_MEASURE(0.01),#23578,
'DISTANCE_ACCURACY_VALUE',
'Maximum model space distance between geometric entities at asserted c
onnectivities');
#23573=(
GEOMETRIC_REPRESENTATION_CONTEXT(3)
GLOBAL_UNCERTAINTY_ASSIGNED_CONTEXT((#23562))
GLOBAL_UNIT_ASSIGNED_CONTEXT((#23578,#23580,#23581))
REPRESENTATION_CONTEXT('','3D')
);
#23577=(
GEOMETRIC_REPRESENTATION_CONTEXT(3)
GLOBAL_UNCERTAINTY_ASSIGNED_CONTEXT((#23566))
GLOBAL_UNIT_ASSIGNED_CONTEXT((#23578,#23580,#23581))
REPRESENTATION_CONTEXT('','3D')
);
#23578=(
LENGTH_UNIT()
NAMED_UNIT(*)
SI_UNIT(.MILLI.,.METRE.)
);
#23580=(
NAMED_UNIT(*)
PLANE_ANGLE_UNIT()
SI_UNIT($,.RADIAN.)
);
#23581=(
NAMED_UNIT(*)
SI_UNIT($,.STERADIAN.)
SOLID_ANGLE_UNIT()
);
#23588=SHAPE_DEFINITION_REPRESENTATION(#23598,#23617);
#23598=PRODUCT_DEFINITION_SHAPE('',$,#23628);
#23617=SHAPE_REPRESENTATION('',(#4473),#23573);
#23621=PRODUCT_DEFINITION_CONTEXT('part definition',#23653,'design');
#23628=PRODUCT_DEFINITION('Nut_02','Nut_02',#23638,#23621);
#23638=PRODUCT_DEFINITION_FORMATION('',$,#23661);
#23653=APPLICATION_CONTEXT(
'Core Data for Automotive Mechanical Design Process');
#23654=PRODUCT_CONTEXT('part definition',#23653,'mechanical');
#23661=PRODUCT('Nut_02','Nut_02',$,(#23654));
#23666=PRESENTATION_STYLE_ASSIGNMENT((#23671));
#23671=SURFACE_STYLE_USAGE(.BOTH.,#23676);
#23676=SURFACE_SIDE_STYLE('',(#23681));
#23681=SURFACE_STYLE_FILL_AREA(#23686);
#23686=FILL_AREA_STYLE('Opaque(210,210,210)',(#23691));
#23691=FILL_AREA_STYLE_COLOUR('Opaque(210,210,210)',#23696);
#23696=COLOUR_RGB('Opaque(210,210,210)', 0.09019608, 0.27058824, 0.51372549);
ENDSEC;
END-ISO-10303-21;
